ISO-10303-21;
HEADER;
/* Generated by software containing ST-Developer
 * from STEP Tools, Inc. (www.steptools.com) 
 */

FILE_DESCRIPTION(
/* description */ ('PAT-001'),
/* implementation_level */ '2;1');

FILE_NAME(
/* name */ 'Slot Nut - M5 for 20 mm Extrusion.step',
/* time_stamp */ '2026-10-29T17:07:15-07:00',
/* author */ (''),
/* organization */ (''),
/* preprocessor_version */ 'ST-DEVELOPER v20.2',
/* originating_system */ 'Autodesk Translation Framework v15.17.0.0',
/* authorisation */ '');

FILE_SCHEMA (('AUTOMOTIVE_DESIGN { 1 0 10303 214 3 1 1 }'));
ENDSEC;

DATA;
#10=MECHANICAL_DESIGN_GEOMETRIC_PRESENTATION_REPRESENTATION('',(#396),#9622);
#33=ELLIPSE('',#5863,0.299389011154384,0.2117);
#34=ELLIPSE('',#5868,0.299389011154384,0.2117);
#338=SHAPE_REPRESENTATION_RELATIONSHIP('SRR','None',#9762,#363);
#363=ADVANCED_BREP_SHAPE_REPRESENTATION('',(#429),#9611);
#396=STYLED_ITEM('',(#9969),#429);
#429=MANIFOLD_SOLID_BREP('Body1',#5221);
#486=FACE_BOUND('',#1263,.T.);
#655=PLANE('',#5862);
#656=PLANE('',#5870);
#657=PLANE('',#5871);
#658=PLANE('',#5872);
#659=PLANE('',#5873);
#660=PLANE('',#5874);
#661=PLANE('',#5875);
#662=PLANE('',#5876);
#663=PLANE('',#5877);
#908=FACE_OUTER_BOUND('',#1253,.T.);
#909=FACE_OUTER_BOUND('',#1254,.T.);
#910=FACE_OUTER_BOUND('',#1255,.T.);
#911=FACE_OUTER_BOUND('',#1256,.T.);
#912=FACE_OUTER_BOUND('',#1257,.T.);
#913=FACE_OUTER_BOUND('',#1258,.T.);
#914=FACE_OUTER_BOUND('',#1259,.T.);
#915=FACE_OUTER_BOUND('',#1260,.T.);
#916=FACE_OUTER_BOUND('',#1261,.T.);
#917=FACE_OUTER_BOUND('',#1262,.T.);
#1253=EDGE_LOOP('',(#4401,#4402,#4403,#4404,#4405,#4406));
#1254=EDGE_LOOP('',(#4407,#4408,#4409,#4410,#4411,#4412,#4413,#4414));
#1255=EDGE_LOOP('',(#4415,#4416,#4417,#4418,#4419));
#1256=EDGE_LOOP('',(#4420,#4421,#4422,#4423));
#1257=EDGE_LOOP('',(#4424,#4425,#4426,#4427,#4428,#4429));
#1258=EDGE_LOOP('',(#4430,#4431,#4432,#4433,#4434,#4435));
#1259=EDGE_LOOP('',(#4436,#4437,#4438,#4439));
#1260=EDGE_LOOP('',(#4440,#4441,#4442,#4443));
#1261=EDGE_LOOP('',(#4444,#4445,#4446,#4447,#4448,#4449));
#1262=EDGE_LOOP('',(#4450,#4451,#4452,#4453));
#1263=EDGE_LOOP('',(#4454));
#1686=LINE('',#9012,#2091);
#1687=LINE('',#9014,#2092);
#1688=LINE('',#9016,#2093);
#1689=LINE('',#9018,#2094);
#1690=LINE('',#9021,#2095);
#1691=LINE('',#9026,#2096);
#1692=LINE('',#9035,#2097);
#1693=LINE('',#9036,#2098);
#1694=LINE('',#9039,#2099);
#1695=LINE('',#9040,#2100);
#1696=LINE('',#9043,#2101);
#1697=LINE('',#9045,#2102);
#1698=LINE('',#9046,#2103);
#1699=LINE('',#9049,#2104);
#1700=LINE('',#9051,#2105);
#1701=LINE('',#9052,#2106);
#1702=LINE('',#9055,#2107);
#1703=LINE('',#9056,#2108);
#1704=LINE('',#9059,#2109);
#1705=LINE('',#9060,#2110);
#1706=LINE('',#9062,#2111);
#2091=VECTOR('',#7103,1.);
#2092=VECTOR('',#7104,1.);
#2093=VECTOR('',#7105,1.);
#2094=VECTOR('',#7106,1.);
#2095=VECTOR('',#7109,1.);
#2096=VECTOR('',#7114,0.21);
#2097=VECTOR('',#7125,1.);
#2098=VECTOR('',#7126,1.);
#2099=VECTOR('',#7129,1.);
#2100=VECTOR('',#7130,1.);
#2101=VECTOR('',#7133,1.);
#2102=VECTOR('',#7134,1.);
#2103=VECTOR('',#7135,1.);
#2104=VECTOR('',#7138,1.);
#2105=VECTOR('',#7139,1.);
#2106=VECTOR('',#7140,1.);
#2107=VECTOR('',#7143,1.);
#2108=VECTOR('',#7144,1.);
#2109=VECTOR('',#7147,1.);
#2110=VECTOR('',#7148,1.);
#2111=VECTOR('',#7151,1.);
#2344=CIRCLE('',#5865,0.2117);
#2345=CIRCLE('',#5866,0.2117);
#2346=CIRCLE('',#5867,0.2117);
#2347=CIRCLE('',#5869,0.2117);
#2724=VERTEX_POINT('',#9010);
#2725=VERTEX_POINT('',#9011);
#2726=VERTEX_POINT('',#9013);
#2727=VERTEX_POINT('',#9015);
#2728=VERTEX_POINT('',#9017);
#2729=VERTEX_POINT('',#9019);
#2730=VERTEX_POINT('',#9023);
#2731=VERTEX_POINT('',#9025);
#2732=VERTEX_POINT('',#9028);
#2733=VERTEX_POINT('',#9030);
#2734=VERTEX_POINT('',#9034);
#2735=VERTEX_POINT('',#9038);
#2736=VERTEX_POINT('',#9042);
#2737=VERTEX_POINT('',#9044);
#2738=VERTEX_POINT('',#9048);
#2739=VERTEX_POINT('',#9050);
#2740=VERTEX_POINT('',#9054);
#2741=VERTEX_POINT('',#9058);
#3304=EDGE_CURVE('',#2724,#2725,#1686,.T.);
#3305=EDGE_CURVE('',#2725,#2726,#1687,.T.);
#3306=EDGE_CURVE('',#2726,#2727,#1688,.T.);
#3307=EDGE_CURVE('',#2727,#2728,#1689,.T.);
#3308=EDGE_CURVE('',#2728,#2729,#33,.T.);
#3309=EDGE_CURVE('',#2729,#2724,#1690,.T.);
#3310=EDGE_CURVE('',#2730,#2728,#2344,.F.);
#3311=EDGE_CURVE('',#2730,#2731,#1691,.T.);
#3312=EDGE_CURVE('',#2731,#2731,#2345,.T.);
#3313=EDGE_CURVE('',#2732,#2730,#2346,.F.);
#3314=EDGE_CURVE('',#2733,#2732,#34,.T.);
#3315=EDGE_CURVE('',#2729,#2733,#2347,.F.);
#3316=EDGE_CURVE('',#2734,#2727,#1692,.T.);
#3317=EDGE_CURVE('',#2732,#2734,#1693,.T.);
#3318=EDGE_CURVE('',#2735,#2733,#1694,.T.);
#3319=EDGE_CURVE('',#2724,#2735,#1695,.T.);
#3320=EDGE_CURVE('',#2734,#2736,#1696,.T.);
#3321=EDGE_CURVE('',#2736,#2737,#1697,.T.);
#3322=EDGE_CURVE('',#2737,#2735,#1698,.T.);
#3323=EDGE_CURVE('',#2737,#2738,#1699,.T.);
#3324=EDGE_CURVE('',#2739,#2738,#1700,.T.);
#3325=EDGE_CURVE('',#2725,#2739,#1701,.T.);
#3326=EDGE_CURVE('',#2736,#2740,#1702,.T.);
#3327=EDGE_CURVE('',#2738,#2740,#1703,.T.);
#3328=EDGE_CURVE('',#2741,#2739,#1704,.T.);
#3329=EDGE_CURVE('',#2726,#2741,#1705,.T.);
#3330=EDGE_CURVE('',#2740,#2741,#1706,.T.);
#4401=ORIENTED_EDGE('',*,*,#3304,.T.);
#4402=ORIENTED_EDGE('',*,*,#3305,.T.);
#4403=ORIENTED_EDGE('',*,*,#3306,.T.);
#4404=ORIENTED_EDGE('',*,*,#3307,.T.);
#4405=ORIENTED_EDGE('',*,*,#3308,.T.);
#4406=ORIENTED_EDGE('',*,*,#3309,.T.);
#4407=ORIENTED_EDGE('',*,*,#3308,.F.);
#4408=ORIENTED_EDGE('',*,*,#3310,.F.);
#4409=ORIENTED_EDGE('',*,*,#3311,.T.);
#4410=ORIENTED_EDGE('',*,*,#3312,.F.);
#4411=ORIENTED_EDGE('',*,*,#3311,.F.);
#4412=ORIENTED_EDGE('',*,*,#3313,.F.);
#4413=ORIENTED_EDGE('',*,*,#3314,.F.);
#4414=ORIENTED_EDGE('',*,*,#3315,.F.);
#4415=ORIENTED_EDGE('',*,*,#3307,.F.);
#4416=ORIENTED_EDGE('',*,*,#3316,.F.);
#4417=ORIENTED_EDGE('',*,*,#3317,.F.);
#4418=ORIENTED_EDGE('',*,*,#3313,.T.);
#4419=ORIENTED_EDGE('',*,*,#3310,.T.);
#4420=ORIENTED_EDGE('',*,*,#3309,.F.);
#4421=ORIENTED_EDGE('',*,*,#3315,.T.);
#4422=ORIENTED_EDGE('',*,*,#3318,.F.);
#4423=ORIENTED_EDGE('',*,*,#3319,.F.);
#4424=ORIENTED_EDGE('',*,*,#3320,.T.);
#4425=ORIENTED_EDGE('',*,*,#3321,.T.);
#4426=ORIENTED_EDGE('',*,*,#3322,.T.);
#4427=ORIENTED_EDGE('',*,*,#3318,.T.);
#4428=ORIENTED_EDGE('',*,*,#3314,.T.);
#4429=ORIENTED_EDGE('',*,*,#3317,.T.);
#4430=ORIENTED_EDGE('',*,*,#3304,.F.);
#4431=ORIENTED_EDGE('',*,*,#3319,.T.);
#4432=ORIENTED_EDGE('',*,*,#3322,.F.);
#4433=ORIENTED_EDGE('',*,*,#3323,.T.);
#4434=ORIENTED_EDGE('',*,*,#3324,.F.);
#4435=ORIENTED_EDGE('',*,*,#3325,.F.);
#4436=ORIENTED_EDGE('',*,*,#3321,.F.);
#4437=ORIENTED_EDGE('',*,*,#3326,.T.);
#4438=ORIENTED_EDGE('',*,*,#3327,.F.);
#4439=ORIENTED_EDGE('',*,*,#3323,.F.);
#4440=ORIENTED_EDGE('',*,*,#3305,.F.);
#4441=ORIENTED_EDGE('',*,*,#3325,.T.);
#4442=ORIENTED_EDGE('',*,*,#3328,.F.);
#4443=ORIENTED_EDGE('',*,*,#3329,.F.);
#4444=ORIENTED_EDGE('',*,*,#3306,.F.);
#4445=ORIENTED_EDGE('',*,*,#3329,.T.);
#4446=ORIENTED_EDGE('',*,*,#3330,.F.);
#4447=ORIENTED_EDGE('',*,*,#3326,.F.);
#4448=ORIENTED_EDGE('',*,*,#3320,.F.);
#4449=ORIENTED_EDGE('',*,*,#3316,.T.);
#4450=ORIENTED_EDGE('',*,*,#3330,.T.);
#4451=ORIENTED_EDGE('',*,*,#3328,.T.);
#4452=ORIENTED_EDGE('',*,*,#3324,.T.);
#4453=ORIENTED_EDGE('',*,*,#3327,.T.);
#4454=ORIENTED_EDGE('',*,*,#3312,.T.);
#4871=CYLINDRICAL_SURFACE('',#5864,0.2117);
#5095=ADVANCED_FACE('',(#908),#655,.T.);
#5096=ADVANCED_FACE('',(#909),#4871,.F.);
#5097=ADVANCED_FACE('',(#910),#656,.F.);
#5098=ADVANCED_FACE('',(#911),#657,.F.);
#5099=ADVANCED_FACE('',(#912),#658,.T.);
#5100=ADVANCED_FACE('',(#913),#659,.T.);
#5101=ADVANCED_FACE('',(#914),#660,.T.);
#5102=ADVANCED_FACE('',(#915),#661,.T.);
#5103=ADVANCED_FACE('',(#916),#662,.T.);
#5104=ADVANCED_FACE('',(#917,#486),#663,.T.);
#5221=CLOSED_SHELL('',(#5095,#5096,#5097,#5098,#5099,#5100,#5101,#5102,
#5103,#5104));
#5861=AXIS2_PLACEMENT_3D('',#9008,#7099,#7100);
#5862=AXIS2_PLACEMENT_3D('',#9009,#7101,#7102);
#5863=AXIS2_PLACEMENT_3D('',#9020,#7107,#7108);
#5864=AXIS2_PLACEMENT_3D('',#9022,#7110,#7111);
#5865=AXIS2_PLACEMENT_3D('',#9024,#7112,#7113);
#5866=AXIS2_PLACEMENT_3D('',#9027,#7115,#7116);
#5867=AXIS2_PLACEMENT_3D('',#9029,#7117,#7118);
#5868=AXIS2_PLACEMENT_3D('',#9031,#7119,#7120);
#5869=AXIS2_PLACEMENT_3D('',#9032,#7121,#7122);
#5870=AXIS2_PLACEMENT_3D('',#9033,#7123,#7124);
#5871=AXIS2_PLACEMENT_3D('',#9037,#7127,#7128);
#5872=AXIS2_PLACEMENT_3D('',#9041,#7131,#7132);
#5873=AXIS2_PLACEMENT_3D('',#9047,#7136,#7137);
#5874=AXIS2_PLACEMENT_3D('',#9053,#7141,#7142);
#5875=AXIS2_PLACEMENT_3D('',#9057,#7145,#7146);
#5876=AXIS2_PLACEMENT_3D('',#9061,#7149,#7150);
#5877=AXIS2_PLACEMENT_3D('',#9063,#7152,#7153);
#7099=DIRECTION('axis',(0.,0.,1.));
#7100=DIRECTION('refdir',(1.,0.,0.));
#7101=DIRECTION('center_axis',(0.,-0.707106781186548,-0.707106781186548));
#7102=DIRECTION('ref_axis',(-1.,0.,0.));
#7103=DIRECTION('',(0.,-0.707106781186548,0.707106781186548));
#7104=DIRECTION('',(-1.,0.,0.));
#7105=DIRECTION('',(0.,0.707106781186548,-0.707106781186548));
#7106=DIRECTION('',(1.,0.,0.));
#7107=DIRECTION('center_axis',(0.,0.707106781186548,0.707106781186548));
#7108=DIRECTION('ref_axis',(0.,0.707106781186547,-0.707106781186547));
#7109=DIRECTION('',(1.,0.,0.));
#7110=DIRECTION('center_axis',(0.,0.,1.));
#7111=DIRECTION('ref_axis',(1.,0.,0.));
#7112=DIRECTION('center_axis',(0.,0.,-1.));
#7113=DIRECTION('ref_axis',(1.,0.,0.));
#7114=DIRECTION('',(0.,0.,1.));
#7115=DIRECTION('center_axis',(0.,0.,-1.));
#7116=DIRECTION('ref_axis',(1.,0.,0.));
#7117=DIRECTION('center_axis',(0.,0.,-1.));
#7118=DIRECTION('ref_axis',(1.,0.,0.));
#7119=DIRECTION('center_axis',(0.,-0.707106781186548,0.707106781186548));
#7120=DIRECTION('ref_axis',(0.,0.707106781186547,0.707106781186547));
#7121=DIRECTION('center_axis',(0.,0.,-1.));
#7122=DIRECTION('ref_axis',(1.,0.,0.));
#7123=DIRECTION('center_axis',(0.,0.,1.));
#7124=DIRECTION('ref_axis',(1.,0.,0.));
#7125=DIRECTION('',(0.,-1.,0.));
#7126=DIRECTION('',(-1.,0.,0.));
#7127=DIRECTION('center_axis',(0.,0.,1.));
#7128=DIRECTION('ref_axis',(1.,0.,0.));
#7129=DIRECTION('',(-1.,0.,0.));
#7130=DIRECTION('',(0.,1.,0.));
#7131=DIRECTION('center_axis',(0.,0.707106781186548,-0.707106781186548));
#7132=DIRECTION('ref_axis',(-1.,0.,0.));
#7133=DIRECTION('',(0.,0.707106781186548,0.707106781186548));
#7134=DIRECTION('',(1.,0.,0.));
#7135=DIRECTION('',(0.,-0.707106781186548,-0.707106781186548));
#7136=DIRECTION('center_axis',(1.,0.,0.));
#7137=DIRECTION('ref_axis',(0.,1.,0.));
#7138=DIRECTION('',(0.,0.,1.));
#7139=DIRECTION('',(0.,1.,0.));
#7140=DIRECTION('',(0.,0.,1.));
#7141=DIRECTION('center_axis',(0.,1.,0.));
#7142=DIRECTION('ref_axis',(-1.,0.,0.));
#7143=DIRECTION('',(0.,0.,1.));
#7144=DIRECTION('',(-1.,0.,0.));
#7145=DIRECTION('center_axis',(0.,-1.,0.));
#7146=DIRECTION('ref_axis',(1.,0.,0.));
#7147=DIRECTION('',(1.,0.,0.));
#7148=DIRECTION('',(0.,0.,1.));
#7149=DIRECTION('center_axis',(-1.,0.,0.));
#7150=DIRECTION('ref_axis',(0.,-1.,0.));
#7151=DIRECTION('',(0.,-1.,0.));
#7152=DIRECTION('center_axis',(0.,0.,1.));
#7153=DIRECTION('ref_axis',(1.,0.,0.));
#9008=CARTESIAN_POINT('',(0.,0.,0.));
#9009=CARTESIAN_POINT('Origin',(-0.25,-0.225,0.075));
#9010=CARTESIAN_POINT('',(0.5,-0.15,0.));
#9011=CARTESIAN_POINT('',(0.5,-0.3,0.15));
#9012=CARTESIAN_POINT('',(0.5,-0.225,0.075));
#9013=CARTESIAN_POINT('',(-0.5,-0.3,0.15));
#9014=CARTESIAN_POINT('',(-0.25,-0.3,0.15));
#9015=CARTESIAN_POINT('',(-0.5,-0.15,0.));
#9016=CARTESIAN_POINT('',(-0.5,-0.075,-0.075));
#9017=CARTESIAN_POINT('',(-0.149388386429468,-0.15,0.));
#9018=CARTESIAN_POINT('',(-0.25,-0.15,0.));
#9019=CARTESIAN_POINT('',(0.149388386429468,-0.15,0.));
#9020=CARTESIAN_POINT('Origin',(0.,0.,-0.15));
#9021=CARTESIAN_POINT('',(-0.25,-0.15,0.));
#9022=CARTESIAN_POINT('Origin',(0.,0.,-0.1));
#9023=CARTESIAN_POINT('',(-0.2117,-2.59257727379495E-17,0.));
#9024=CARTESIAN_POINT('Origin',(0.,0.,0.));
#9025=CARTESIAN_POINT('',(-0.2117,2.59257727379495E-17,0.4));
#9026=CARTESIAN_POINT('',(-0.2117,-2.59257727379495E-17,-0.1));
#9027=CARTESIAN_POINT('Origin',(0.,0.,0.4));
#9028=CARTESIAN_POINT('',(-0.149388386429468,0.15,0.));
#9029=CARTESIAN_POINT('Origin',(0.,0.,0.));
#9030=CARTESIAN_POINT('',(0.149388386429468,0.15,0.));
#9031=CARTESIAN_POINT('Origin',(0.,0.,-0.15));
#9032=CARTESIAN_POINT('Origin',(0.,0.,0.));
#9033=CARTESIAN_POINT('Origin',(0.,0.,0.));
#9034=CARTESIAN_POINT('',(-0.5,0.15,0.));
#9035=CARTESIAN_POINT('',(-0.5,0.3,0.));
#9036=CARTESIAN_POINT('',(0.25,0.15,0.));
#9037=CARTESIAN_POINT('Origin',(0.,0.,0.));
#9038=CARTESIAN_POINT('',(0.5,0.15,0.));
#9039=CARTESIAN_POINT('',(0.25,0.15,0.));
#9040=CARTESIAN_POINT('',(0.5,-0.3,0.));
#9041=CARTESIAN_POINT('Origin',(0.25,0.225,0.075));
#9042=CARTESIAN_POINT('',(-0.5,0.3,0.15));
#9043=CARTESIAN_POINT('',(-0.5,0.225,0.075));
#9044=CARTESIAN_POINT('',(0.5,0.3,0.15));
#9045=CARTESIAN_POINT('',(0.25,0.3,0.15));
#9046=CARTESIAN_POINT('',(0.5,0.075,-0.075));
#9047=CARTESIAN_POINT('Origin',(0.5,-0.3,0.));
#9048=CARTESIAN_POINT('',(0.5,0.3,0.4));
#9049=CARTESIAN_POINT('',(0.5,0.3,0.));
#9050=CARTESIAN_POINT('',(0.5,-0.3,0.4));
#9051=CARTESIAN_POINT('',(0.5,-0.3,0.4));
#9052=CARTESIAN_POINT('',(0.5,-0.3,0.));
#9053=CARTESIAN_POINT('Origin',(0.5,0.3,0.));
#9054=CARTESIAN_POINT('',(-0.5,0.3,0.4));
#9055=CARTESIAN_POINT('',(-0.5,0.3,0.));
#9056=CARTESIAN_POINT('',(0.5,0.3,0.4));
#9057=CARTESIAN_POINT('Origin',(-0.5,-0.3,0.));
#9058=CARTESIAN_POINT('',(-0.5,-0.3,0.4));
#9059=CARTESIAN_POINT('',(-0.5,-0.3,0.4));
#9060=CARTESIAN_POINT('',(-0.5,-0.3,0.));
#9061=CARTESIAN_POINT('Origin',(-0.5,0.3,0.));
#9062=CARTESIAN_POINT('',(-0.5,0.3,0.4));
#9063=CARTESIAN_POINT('Origin',(0.,0.,0.4));
#9581=UNCERTAINTY_MEASURE_WITH_UNIT(LENGTH_MEASURE(0.001),#9623,
'DISTANCE_ACCURACY_VALUE',
'Maximum model space distance between geometric entities at asserted c
onnectivities');
#9592=UNCERTAINTY_MEASURE_WITH_UNIT(LENGTH_MEASURE(0.001),#9623,
'DISTANCE_ACCURACY_VALUE',
'Maximum model space distance between geometric entities at asserted c
onnectivities');
#9611=(
GEOMETRIC_REPRESENTATION_CONTEXT(3)
GLOBAL_UNCERTAINTY_ASSIGNED_CONTEXT((#9581))
GLOBAL_UNIT_ASSIGNED_CONTEXT((#9623,#9625,#9626))
REPRESENTATION_CONTEXT('','3D')
);
#9622=(
GEOMETRIC_REPRESENTATION_CONTEXT(3)
GLOBAL_UNCERTAINTY_ASSIGNED_CONTEXT((#9592))
GLOBAL_UNIT_ASSIGNED_CONTEXT((#9623,#9625,#9626))
REPRESENTATION_CONTEXT('','3D')
);
#9623=(
LENGTH_UNIT()
NAMED_UNIT(*)
SI_UNIT(.CENTI.,.METRE.)
);
#9625=(
NAMED_UNIT(*)
PLANE_ANGLE_UNIT()
SI_UNIT($,.RADIAN.)
);
#9626=(
NAMED_UNIT(*)
SI_UNIT($,.STERADIAN.)
SOLID_ANGLE_UNIT()
);
#9645=SHAPE_DEFINITION_REPRESENTATION(#9679,#9762);
#9679=PRODUCT_DEFINITION_SHAPE('',$,#9792);
#9762=SHAPE_REPRESENTATION('',(#5861),#9611);
#9773=PRODUCT_DEFINITION_CONTEXT('part definition',#9862,'design');
#9792=PRODUCT_DEFINITION('Slot Nut - M5 for 20 mm Extrusion',
'Slot Nut - M5 for 20 mm Extrusion',#9821,#9773);
#9821=PRODUCT_DEFINITION_FORMATION('',$,#9882);
#9862=APPLICATION_CONTEXT(
'Core Data for Automotive Mechanical Design Process');
#9863=PRODUCT_CONTEXT('part definition',#9862,'mechanical');
#9882=PRODUCT('Slot Nut - M5 for 20 mm Extrusion',
'Slot Nut - M5 for 20 mm Extrusion','Slot Nut - M5 for 20 mm Extrusion',
(#9863));
#9963=COLOUR_RGB('Black',0.12,0.14,0.17);
#9964=FILL_AREA_STYLE_COLOUR('',#9963);
#9965=FILL_AREA_STYLE('',(#9964));
#9966=SURFACE_STYLE_FILL_AREA(#9965);
#9967=SURFACE_SIDE_STYLE('',(#9966));
#9968=SURFACE_STYLE_USAGE(.BOTH.,#9967);
#9969=PRESENTATION_STYLE_ASSIGNMENT((#9968));
ENDSEC;
END-ISO-10303-21;
